ISO-10303-21;
HEADER;
/* Generated by software containing ST-Developer
 * from STEP Tools, Inc. (www.steptools.com) 
 */

FILE_DESCRIPTION(
/* description */ ('Bin tilter linkage'),
/* implementation_level */ '2;1');

FILE_NAME(
/* name */ 'Cap Screw - M4x16.step',
/* time_stamp */ '2026-10-28T03:26:24-07:00',
/* author */ (''),
/* organization */ (''),
/* preprocessor_version */ 'ST-DEVELOPER v20.2',
/* originating_system */ 'Autodesk Translation Framework v15.17.0.0',
/* authorisation */ '');

FILE_SCHEMA (('AUTOMOTIVE_DESIGN { 1 0 10303 214 3 1 1 }'));
ENDSEC;

DATA;
#10=MECHANICAL_DESIGN_GEOMETRIC_PRESENTATION_REPRESENTATION('',(#959),#23728);
#630=ORIENTED_CLOSED_SHELL('',*,#12491,.F.);
#640=CONICAL_SURFACE('',#15132,0.325,0.785398163397448);
#641=CONICAL_SURFACE('',#15136,0.335,0.785398163397448);
#642=CONICAL_SURFACE('',#15140,0.21,0.463647609000806);
#643=CONICAL_SURFACE('',#15144,0.18,0.785398163397448);
#648=BREP_WITH_VOIDS('Body1',#12490,(#630));
#739=SHAPE_REPRESENTATION_RELATIONSHIP('SRR','None',#24207,#845);
#845=ADVANCED_BREP_SHAPE_REPRESENTATION('',(#648),#23707);
#959=STYLED_ITEM('',(#24772),#648);
#1443=FACE_BOUND('',#3672,.T.);
#1805=PLANE('',#15130);
#1806=PLANE('',#15138);
#1807=PLANE('',#15146);
#1808=PLANE('',#15147);
#1809=PLANE('',#15148);
#1810=PLANE('',#15149);
#1811=PLANE('',#15150);
#1812=PLANE('',#15151);
#1813=PLANE('',#15152);
#1814=PLANE('',#15153);
#1815=PLANE('',#15154);
#2534=FACE_OUTER_BOUND('',#3667,.T.);
#2535=FACE_OUTER_BOUND('',#3668,.T.);
#2536=FACE_OUTER_BOUND('',#3669,.T.);
#2537=FACE_OUTER_BOUND('',#3670,.T.);
#2538=FACE_OUTER_BOUND('',#3671,.T.);
#2539=FACE_OUTER_BOUND('',#3673,.T.);
#2540=FACE_OUTER_BOUND('',#3674,.T.);
#2541=FACE_OUTER_BOUND('',#3675,.T.);
#2542=FACE_OUTER_BOUND('',#3676,.T.);
#2543=FACE_OUTER_BOUND('',#3677,.T.);
#2544=FACE_OUTER_BOUND('',#3678,.T.);
#2545=FACE_OUTER_BOUND('',#3679,.T.);
#2546=FACE_OUTER_BOUND('',#3680,.T.);
#2547=FACE_OUTER_BOUND('',#3681,.T.);
#2548=FACE_OUTER_BOUND('',#3682,.T.);
#2549=FACE_OUTER_BOUND('',#3683,.T.);
#2550=FACE_OUTER_BOUND('',#3684,.T.);
#3667=EDGE_LOOP('',(#10765));
#3668=EDGE_LOOP('',(#10766,#10767,#10768,#10769));
#3669=EDGE_LOOP('',(#10770,#10771,#10772,#10773));
#3670=EDGE_LOOP('',(#10774,#10775,#10776,#10777));
#3671=EDGE_LOOP('',(#10778));
#3672=EDGE_LOOP('',(#10779));
#3673=EDGE_LOOP('',(#10780,#10781,#10782,#10783));
#3674=EDGE_LOOP('',(#10784,#10785,#10786,#10787));
#3675=EDGE_LOOP('',(#10788,#10789,#10790,#10791));
#3676=EDGE_LOOP('',(#10792));
#3677=EDGE_LOOP('',(#10793,#10794,#10795,#10796));
#3678=EDGE_LOOP('',(#10797,#10798,#10799,#10800));
#3679=EDGE_LOOP('',(#10801,#10802,#10803,#10804));
#3680=EDGE_LOOP('',(#10805,#10806,#10807,#10808));
#3681=EDGE_LOOP('',(#10809,#10810,#10811,#10812));
#3682=EDGE_LOOP('',(#10813,#10814,#10815,#10816));
#3683=EDGE_LOOP('',(#10817,#10818,#10819,#10820,#10821,#10822));
#3684=EDGE_LOOP('',(#10823,#10824,#10825,#10826,#10827,#10828));
#4368=LINE('',#22836,#5043);
#4369=LINE('',#22840,#5044);
#4370=LINE('',#22844,#5045);
#4371=LINE('',#22851,#5046);
#4372=LINE('',#22855,#5047);
#4373=LINE('',#22859,#5048);
#4374=LINE('',#22864,#5049);
#4375=LINE('',#22866,#5050);
#4376=LINE('',#22868,#5051);
#4377=LINE('',#22869,#5052);
#4378=LINE('',#22872,#5053);
#4379=LINE('',#22874,#5054);
#4380=LINE('',#22875,#5055);
#4381=LINE('',#22878,#5056);
#4382=LINE('',#22880,#5057);
#4383=LINE('',#22881,#5058);
#4384=LINE('',#22884,#5059);
#4385=LINE('',#22886,#5060);
#4386=LINE('',#22887,#5061);
#4387=LINE('',#22890,#5062);
#4388=LINE('',#22892,#5063);
#4389=LINE('',#22893,#5064);
#4390=LINE('',#22895,#5065);
#4391=LINE('',#22896,#5066);
#5043=VECTOR('',#18909,0.325);
#5044=VECTOR('',#18914,0.35);
#5045=VECTOR('',#18919,0.335);
#5046=VECTOR('',#18928,0.21);
#5047=VECTOR('',#18933,0.2);
#5048=VECTOR('',#18938,0.18);
#5049=VECTOR('',#18943,1.);
#5050=VECTOR('',#18944,1.);
#5051=VECTOR('',#18945,1.);
#5052=VECTOR('',#18946,1.);
#5053=VECTOR('',#18949,1.);
#5054=VECTOR('',#18950,1.);
#5055=VECTOR('',#18951,1.);
#5056=VECTOR('',#18954,1.);
#5057=VECTOR('',#18955,1.);
#5058=VECTOR('',#18956,1.);
#5059=VECTOR('',#18959,1.);
#5060=VECTOR('',#18960,1.);
#5061=VECTOR('',#18961,1.);
#5062=VECTOR('',#18964,1.);
#5063=VECTOR('',#18965,1.);
#5064=VECTOR('',#18966,1.);
#5065=VECTOR('',#18969,1.);
#5066=VECTOR('',#18970,1.);
#5862=CIRCLE('',#15131,0.3);
#5863=CIRCLE('',#15133,0.35);
#5864=CIRCLE('',#15135,0.35);
#5865=CIRCLE('',#15137,0.32);
#5866=CIRCLE('',#15139,0.22);
#5867=CIRCLE('',#15141,0.1954);
#5868=CIRCLE('',#15143,0.1954);
#5869=CIRCLE('',#15145,0.16);
#6761=VERTEX_POINT('',#22831);
#6762=VERTEX_POINT('',#22834);
#6763=VERTEX_POINT('',#22838);
#6764=VERTEX_POINT('',#22842);
#6765=VERTEX_POINT('',#22846);
#6766=VERTEX_POINT('',#22849);
#6767=VERTEX_POINT('',#22853);
#6768=VERTEX_POINT('',#22857);
#6769=VERTEX_POINT('',#22862);
#6770=VERTEX_POINT('',#22863);
#6771=VERTEX_POINT('',#22865);
#6772=VERTEX_POINT('',#22867);
#6773=VERTEX_POINT('',#22871);
#6774=VERTEX_POINT('',#22873);
#6775=VERTEX_POINT('',#22877);
#6776=VERTEX_POINT('',#22879);
#6777=VERTEX_POINT('',#22883);
#6778=VERTEX_POINT('',#22885);
#6779=VERTEX_POINT('',#22889);
#6780=VERTEX_POINT('',#22891);
#8122=EDGE_CURVE('',#6761,#6761,#5862,.T.);
#8123=EDGE_CURVE('',#6762,#6762,#5863,.T.);
#8124=EDGE_CURVE('',#6762,#6761,#4368,.T.);
#8125=EDGE_CURVE('',#6763,#6763,#5864,.T.);
#8126=EDGE_CURVE('',#6763,#6762,#4369,.T.);
#8127=EDGE_CURVE('',#6764,#6764,#5865,.T.);
#8128=EDGE_CURVE('',#6764,#6763,#4370,.T.);
#8129=EDGE_CURVE('',#6765,#6765,#5866,.T.);
#8130=EDGE_CURVE('',#6766,#6766,#5867,.F.);
#8131=EDGE_CURVE('',#6766,#6765,#4371,.T.);
#8132=EDGE_CURVE('',#6767,#6767,#5868,.F.);
#8133=EDGE_CURVE('',#6767,#6766,#4372,.T.);
#8134=EDGE_CURVE('',#6768,#6768,#5869,.T.);
#8135=EDGE_CURVE('',#6768,#6767,#4373,.T.);
#8136=EDGE_CURVE('',#6769,#6770,#4374,.T.);
#8137=EDGE_CURVE('',#6770,#6771,#4375,.T.);
#8138=EDGE_CURVE('',#6771,#6772,#4376,.T.);
#8139=EDGE_CURVE('',#6769,#6772,#4377,.T.);
#8140=EDGE_CURVE('',#6770,#6773,#4378,.T.);
#8141=EDGE_CURVE('',#6773,#6774,#4379,.T.);
#8142=EDGE_CURVE('',#6774,#6771,#4380,.T.);
#8143=EDGE_CURVE('',#6773,#6775,#4381,.T.);
#8144=EDGE_CURVE('',#6775,#6776,#4382,.T.);
#8145=EDGE_CURVE('',#6776,#6774,#4383,.T.);
#8146=EDGE_CURVE('',#6775,#6777,#4384,.T.);
#8147=EDGE_CURVE('',#6777,#6778,#4385,.T.);
#8148=EDGE_CURVE('',#6778,#6776,#4386,.T.);
#8149=EDGE_CURVE('',#6777,#6779,#4387,.T.);
#8150=EDGE_CURVE('',#6779,#6780,#4388,.T.);
#8151=EDGE_CURVE('',#6780,#6778,#4389,.T.);
#8152=EDGE_CURVE('',#6779,#6769,#4390,.T.);
#8153=EDGE_CURVE('',#6772,#6780,#4391,.T.);
#10765=ORIENTED_EDGE('',*,*,#8122,.F.);
#10766=ORIENTED_EDGE('',*,*,#8123,.F.);
#10767=ORIENTED_EDGE('',*,*,#8124,.T.);
#10768=ORIENTED_EDGE('',*,*,#8122,.T.);
#10769=ORIENTED_EDGE('',*,*,#8124,.F.);
#10770=ORIENTED_EDGE('',*,*,#8125,.F.);
#10771=ORIENTED_EDGE('',*,*,#8126,.T.);
#10772=ORIENTED_EDGE('',*,*,#8123,.T.);
#10773=ORIENTED_EDGE('',*,*,#8126,.F.);
#10774=ORIENTED_EDGE('',*,*,#8127,.F.);
#10775=ORIENTED_EDGE('',*,*,#8128,.T.);
#10776=ORIENTED_EDGE('',*,*,#8125,.T.);
#10777=ORIENTED_EDGE('',*,*,#8128,.F.);
#10778=ORIENTED_EDGE('',*,*,#8127,.T.);
#10779=ORIENTED_EDGE('',*,*,#8129,.F.);
#10780=ORIENTED_EDGE('',*,*,#8130,.F.);
#10781=ORIENTED_EDGE('',*,*,#8131,.T.);
#10782=ORIENTED_EDGE('',*,*,#8129,.T.);
#10783=ORIENTED_EDGE('',*,*,#8131,.F.);
#10784=ORIENTED_EDGE('',*,*,#8132,.F.);
#10785=ORIENTED_EDGE('',*,*,#8133,.T.);
#10786=ORIENTED_EDGE('',*,*,#8130,.T.);
#10787=ORIENTED_EDGE('',*,*,#8133,.F.);
#10788=ORIENTED_EDGE('',*,*,#8134,.F.);
#10789=ORIENTED_EDGE('',*,*,#8135,.T.);
#10790=ORIENTED_EDGE('',*,*,#8132,.T.);
#10791=ORIENTED_EDGE('',*,*,#8135,.F.);
#10792=ORIENTED_EDGE('',*,*,#8134,.T.);
#10793=ORIENTED_EDGE('',*,*,#8136,.T.);
#10794=ORIENTED_EDGE('',*,*,#8137,.T.);
#10795=ORIENTED_EDGE('',*,*,#8138,.T.);
#10796=ORIENTED_EDGE('',*,*,#8139,.F.);
#10797=ORIENTED_EDGE('',*,*,#8140,.T.);
#10798=ORIENTED_EDGE('',*,*,#8141,.T.);
#10799=ORIENTED_EDGE('',*,*,#8142,.T.);
#10800=ORIENTED_EDGE('',*,*,#8137,.F.);
#10801=ORIENTED_EDGE('',*,*,#8143,.T.);
#10802=ORIENTED_EDGE('',*,*,#8144,.T.);
#10803=ORIENTED_EDGE('',*,*,#8145,.T.);
#10804=ORIENTED_EDGE('',*,*,#8141,.F.);
#10805=ORIENTED_EDGE('',*,*,#8146,.T.);
#10806=ORIENTED_EDGE('',*,*,#8147,.T.);
#10807=ORIENTED_EDGE('',*,*,#8148,.T.);
#10808=ORIENTED_EDGE('',*,*,#8144,.F.);
#10809=ORIENTED_EDGE('',*,*,#8149,.T.);
#10810=ORIENTED_EDGE('',*,*,#8150,.T.);
#10811=ORIENTED_EDGE('',*,*,#8151,.T.);
#10812=ORIENTED_EDGE('',*,*,#8147,.F.);
#10813=ORIENTED_EDGE('',*,*,#8152,.T.);
#10814=ORIENTED_EDGE('',*,*,#8139,.T.);
#10815=ORIENTED_EDGE('',*,*,#8153,.T.);
#10816=ORIENTED_EDGE('',*,*,#8150,.F.);
#10817=ORIENTED_EDGE('',*,*,#8152,.F.);
#10818=ORIENTED_EDGE('',*,*,#8149,.F.);
#10819=ORIENTED_EDGE('',*,*,#8146,.F.);
#10820=ORIENTED_EDGE('',*,*,#8143,.F.);
#10821=ORIENTED_EDGE('',*,*,#8140,.F.);
#10822=ORIENTED_EDGE('',*,*,#8136,.F.);
#10823=ORIENTED_EDGE('',*,*,#8153,.F.);
#10824=ORIENTED_EDGE('',*,*,#8138,.F.);
#10825=ORIENTED_EDGE('',*,*,#8142,.F.);
#10826=ORIENTED_EDGE('',*,*,#8145,.F.);
#10827=ORIENTED_EDGE('',*,*,#8148,.F.);
#10828=ORIENTED_EDGE('',*,*,#8151,.F.);
#11574=CYLINDRICAL_SURFACE('',#15134,0.35);
#11575=CYLINDRICAL_SURFACE('',#15142,0.1954);
#12259=ADVANCED_FACE('',(#2534),#1805,.T.);
#12260=ADVANCED_FACE('',(#2535),#640,.T.);
#12261=ADVANCED_FACE('',(#2536),#11574,.T.);
#12262=ADVANCED_FACE('',(#2537),#641,.T.);
#12263=ADVANCED_FACE('',(#2538,#1443),#1806,.T.);
#12264=ADVANCED_FACE('',(#2539),#642,.T.);
#12265=ADVANCED_FACE('',(#2540),#11575,.T.);
#12266=ADVANCED_FACE('',(#2541),#643,.T.);
#12267=ADVANCED_FACE('',(#2542),#1807,.T.);
#12268=ADVANCED_FACE('',(#2543),#1808,.F.);
#12269=ADVANCED_FACE('',(#2544),#1809,.F.);
#12270=ADVANCED_FACE('',(#2545),#1810,.F.);
#12271=ADVANCED_FACE('',(#2546),#1811,.F.);
#12272=ADVANCED_FACE('',(#2547),#1812,.F.);
#12273=ADVANCED_FACE('',(#2548),#1813,.F.);
#12274=ADVANCED_FACE('',(#2549),#1814,.F.);
#12275=ADVANCED_FACE('',(#2550),#1815,.F.);
#12490=CLOSED_SHELL('',(#12259,#12260,#12261,#12262,#12263,#12264,#12265,
#12266,#12267));
#12491=CLOSED_SHELL('',(#12268,#12269,#12270,#12271,#12272,#12273,#12274,
#12275));
#15129=AXIS2_PLACEMENT_3D('',#22829,#18899,#18900);
#15130=AXIS2_PLACEMENT_3D('',#22830,#18901,#18902);
#15131=AXIS2_PLACEMENT_3D('',#22832,#18903,#18904);
#15132=AXIS2_PLACEMENT_3D('',#22833,#18905,#18906);
#15133=AXIS2_PLACEMENT_3D('',#22835,#18907,#18908);
#15134=AXIS2_PLACEMENT_3D('',#22837,#18910,#18911);
#15135=AXIS2_PLACEMENT_3D('',#22839,#18912,#18913);
#15136=AXIS2_PLACEMENT_3D('',#22841,#18915,#18916);
#15137=AXIS2_PLACEMENT_3D('',#22843,#18917,#18918);
#15138=AXIS2_PLACEMENT_3D('',#22845,#18920,#18921);
#15139=AXIS2_PLACEMENT_3D('',#22847,#18922,#18923);
#15140=AXIS2_PLACEMENT_3D('',#22848,#18924,#18925);
#15141=AXIS2_PLACEMENT_3D('',#22850,#18926,#18927);
#15142=AXIS2_PLACEMENT_3D('',#22852,#18929,#18930);
#15143=AXIS2_PLACEMENT_3D('',#22854,#18931,#18932);
#15144=AXIS2_PLACEMENT_3D('',#22856,#18934,#18935);
#15145=AXIS2_PLACEMENT_3D('',#22858,#18936,#18937);
#15146=AXIS2_PLACEMENT_3D('',#22860,#18939,#18940);
#15147=AXIS2_PLACEMENT_3D('',#22861,#18941,#18942);
#15148=AXIS2_PLACEMENT_3D('',#22870,#18947,#18948);
#15149=AXIS2_PLACEMENT_3D('',#22876,#18952,#18953);
#15150=AXIS2_PLACEMENT_3D('',#22882,#18957,#18958);
#15151=AXIS2_PLACEMENT_3D('',#22888,#18962,#18963);
#15152=AXIS2_PLACEMENT_3D('',#22894,#18967,#18968);
#15153=AXIS2_PLACEMENT_3D('',#22897,#18971,#18972);
#15154=AXIS2_PLACEMENT_3D('',#22898,#18973,#18974);
#18899=DIRECTION('axis',(0.,0.,1.));
#18900=DIRECTION('refdir',(1.,0.,0.));
#18901=DIRECTION('center_axis',(0.,1.,0.));
#18902=DIRECTION('ref_axis',(0.,0.,1.));
#18903=DIRECTION('center_axis',(0.,-1.,0.));
#18904=DIRECTION('ref_axis',(1.,0.,0.));
#18905=DIRECTION('center_axis',(0.,-1.,0.));
#18906=DIRECTION('ref_axis',(1.,0.,0.));
#18907=DIRECTION('center_axis',(0.,-1.,0.));
#18908=DIRECTION('ref_axis',(1.,0.,0.));
#18909=DIRECTION('',(0.707106781186547,0.707106781186548,8.65956056235493E-17));
#18910=DIRECTION('center_axis',(0.,-1.,0.));
#18911=DIRECTION('ref_axis',(1.,0.,0.));
#18912=DIRECTION('center_axis',(0.,-1.,0.));
#18913=DIRECTION('ref_axis',(1.,0.,0.));
#18914=DIRECTION('',(0.,1.,0.));
#18915=DIRECTION('center_axis',(0.,1.,0.));
#18916=DIRECTION('ref_axis',(1.,0.,0.));
#18917=DIRECTION('center_axis',(0.,-1.,0.));
#18918=DIRECTION('ref_axis',(1.,0.,0.));
#18919=DIRECTION('',(-0.707106781186547,0.707106781186548,-8.65956056235493E-17));
#18920=DIRECTION('center_axis',(0.,-1.,0.));
#18921=DIRECTION('ref_axis',(0.,0.,-1.));
#18922=DIRECTION('center_axis',(0.,-1.,0.));
#18923=DIRECTION('ref_axis',(1.,0.,0.));
#18924=DIRECTION('center_axis',(0.,1.,0.));
#18925=DIRECTION('ref_axis',(1.,0.,0.));
#18926=DIRECTION('center_axis',(0.,1.,0.));
#18927=DIRECTION('ref_axis',(1.,0.,0.));
#18928=DIRECTION('',(-0.447213595499958,0.894427190999916,-5.47678698264203E-17));
#18929=DIRECTION('center_axis',(0.,-1.,0.));
#18930=DIRECTION('ref_axis',(1.,0.,0.));
#18931=DIRECTION('center_axis',(0.,1.,0.));
#18932=DIRECTION('ref_axis',(1.,0.,0.));
#18933=DIRECTION('',(0.,1.,0.));
#18934=DIRECTION('center_axis',(0.,1.,0.));
#18935=DIRECTION('ref_axis',(1.,0.,0.));
#18936=DIRECTION('center_axis',(0.,-1.,0.));
#18937=DIRECTION('ref_axis',(1.,0.,0.));
#18938=DIRECTION('',(-0.707106781186547,0.707106781186548,-8.65956056235493E-17));
#18939=DIRECTION('center_axis',(0.,-1.,0.));
#18940=DIRECTION('ref_axis',(0.,0.,-1.));
#18941=DIRECTION('center_axis',(0.866025403784439,0.,-0.5));
#18942=DIRECTION('ref_axis',(0.5,0.,0.866025403784439));
#18943=DIRECTION('',(-0.5,0.,-0.866025403784439));
#18944=DIRECTION('',(0.,-1.,0.));
#18945=DIRECTION('',(0.5,0.,0.866025403784439));
#18946=DIRECTION('',(0.,-1.,0.));
#18947=DIRECTION('center_axis',(1.60246890531964E-16,0.,-1.));
#18948=DIRECTION('ref_axis',(1.,0.,1.60246890531964E-16));
#18949=DIRECTION('',(-1.,0.,-1.60246890531964E-16));
#18950=DIRECTION('',(0.,-1.,0.));
#18951=DIRECTION('',(1.,0.,1.60246890531964E-16));
#18952=DIRECTION('center_axis',(-0.866025403784439,0.,-0.5));
#18953=DIRECTION('ref_axis',(0.5,0.,-0.866025403784439));
#18954=DIRECTION('',(-0.5,0.,0.866025403784439));
#18955=DIRECTION('',(0.,-1.,0.));
#18956=DIRECTION('',(0.5,0.,-0.866025403784439));
#18957=DIRECTION('center_axis',(-0.866025403784439,0.,0.5));
#18958=DIRECTION('ref_axis',(-0.5,0.,-0.866025403784439));
#18959=DIRECTION('',(0.5,0.,0.866025403784439));
#18960=DIRECTION('',(0.,-1.,0.));
#18961=DIRECTION('',(-0.5,0.,-0.866025403784439));
#18962=DIRECTION('center_axis',(-1.60246890531964E-16,0.,1.));
#18963=DIRECTION('ref_axis',(-1.,0.,-1.60246890531964E-16));
#18964=DIRECTION('',(1.,0.,1.60246890531964E-16));
#18965=DIRECTION('',(0.,-1.,0.));
#18966=DIRECTION('',(-1.,0.,-1.60246890531964E-16));
#18967=DIRECTION('center_axis',(0.866025403784439,0.,0.5));
#18968=DIRECTION('ref_axis',(-0.5,0.,0.866025403784439));
#18969=DIRECTION('',(0.5,0.,-0.866025403784439));
#18970=DIRECTION('',(-0.5,0.,0.866025403784439));
#18971=DIRECTION('center_axis',(0.,1.,0.));
#18972=DIRECTION('ref_axis',(1.,0.,0.));
#18973=DIRECTION('center_axis',(0.,-1.,0.));
#18974=DIRECTION('ref_axis',(0.,0.,-1.));
#22829=CARTESIAN_POINT('',(0.,0.,0.));
#22830=CARTESIAN_POINT('Origin',(0.3,0.4,0.));
#22831=CARTESIAN_POINT('',(-0.3,0.4,-3.67394039744206E-17));
#22832=CARTESIAN_POINT('Origin',(0.,0.4,0.));
#22833=CARTESIAN_POINT('Origin',(0.,0.375,0.));
#22834=CARTESIAN_POINT('',(-0.35,0.35,-4.28626379701573E-17));
#22835=CARTESIAN_POINT('Origin',(0.,0.35,0.));
#22836=CARTESIAN_POINT('',(-0.325,0.375,-3.9801020972289E-17));
#22837=CARTESIAN_POINT('Origin',(0.,0.19,0.));
#22838=CARTESIAN_POINT('',(-0.35,0.03,-4.28626379701574E-17));
#22839=CARTESIAN_POINT('Origin',(0.,0.03,0.));
#22840=CARTESIAN_POINT('',(-0.35,0.19,-4.28626379701574E-17));
#22841=CARTESIAN_POINT('Origin',(0.,0.0149999999999999,0.));
#22842=CARTESIAN_POINT('',(-0.32,-3.29597460435593E-17,-3.91886975727153E-17));
#22843=CARTESIAN_POINT('Origin',(0.,0.,0.));
#22844=CARTESIAN_POINT('',(-0.335,0.0149999999999999,-4.10256677714363E-17));
#22845=CARTESIAN_POINT('Origin',(0.22,0.,0.));
#22846=CARTESIAN_POINT('',(-0.22,-6.93889390390723E-18,-2.69422295812418E-17));
#22847=CARTESIAN_POINT('Origin',(0.,0.,0.));
#22848=CARTESIAN_POINT('Origin',(0.,-0.02,0.));
#22849=CARTESIAN_POINT('',(-0.1954,-0.0492,2.39295984553393E-17));
#22850=CARTESIAN_POINT('Origin',(0.,-0.0492,0.));
#22851=CARTESIAN_POINT('',(-0.21,-0.02,-2.57175827820944E-17));
#22852=CARTESIAN_POINT('Origin',(0.,-0.8,0.));
#22853=CARTESIAN_POINT('',(-0.1954,-1.5646,2.39295984553393E-17));
#22854=CARTESIAN_POINT('Origin',(0.,-1.5646,0.));
#22855=CARTESIAN_POINT('',(-0.1954,-0.8,-2.39295984553393E-17));
#22856=CARTESIAN_POINT('Origin',(0.,-1.58,0.));
#22857=CARTESIAN_POINT('',(-0.16,-1.6,-1.95943487863577E-17));
#22858=CARTESIAN_POINT('Origin',(0.,-1.6,0.));
#22859=CARTESIAN_POINT('',(-0.18,-1.58,-2.20436423846524E-17));
#22860=CARTESIAN_POINT('Origin',(0.,-1.6,0.));
#22861=CARTESIAN_POINT('Origin',(0.0866025403784439,-0.4,-0.15));
#22862=CARTESIAN_POINT('',(0.173205080756888,-0.4,0.));
#22863=CARTESIAN_POINT('',(0.0866025403784439,-0.4,-0.15));
#22864=CARTESIAN_POINT('',(0.173205080756888,-0.4,0.));
#22865=CARTESIAN_POINT('',(0.0866025403784439,-0.64,-0.15));
#22866=CARTESIAN_POINT('',(0.0866025403784439,-0.4,-0.15));
#22867=CARTESIAN_POINT('',(0.173205080756888,-0.64,0.));
#22868=CARTESIAN_POINT('',(0.173205080756888,-0.64,0.));
#22869=CARTESIAN_POINT('',(0.173205080756888,-0.4,0.));
#22870=CARTESIAN_POINT('Origin',(-0.0866025403784438,-0.4,-0.15));
#22871=CARTESIAN_POINT('',(-0.0866025403784438,-0.4,-0.15));
#22872=CARTESIAN_POINT('',(0.0866025403784439,-0.4,-0.15));
#22873=CARTESIAN_POINT('',(-0.0866025403784438,-0.64,-0.15));
#22874=CARTESIAN_POINT('',(-0.0866025403784438,-0.4,-0.15));
#22875=CARTESIAN_POINT('',(0.0866025403784439,-0.64,-0.15));
#22876=CARTESIAN_POINT('Origin',(-0.173205080756888,-0.4,-2.77555756156289E-17));
#22877=CARTESIAN_POINT('',(-0.173205080756888,-0.4,-2.12115047744981E-17));
#22878=CARTESIAN_POINT('',(-0.0866025403784438,-0.4,-0.15));
#22879=CARTESIAN_POINT('',(-0.173205080756888,-0.64,-2.77555756156289E-17));
#22880=CARTESIAN_POINT('',(-0.173205080756888,-0.4,-2.12115047744981E-17));
#22881=CARTESIAN_POINT('',(-0.0866025403784438,-0.64,-0.15));
#22882=CARTESIAN_POINT('Origin',(-0.0866025403784439,-0.4,0.15));
#22883=CARTESIAN_POINT('',(-0.0866025403784439,-0.4,0.15));
#22884=CARTESIAN_POINT('',(-0.173205080756888,-0.4,-2.12115047744981E-17));
#22885=CARTESIAN_POINT('',(-0.0866025403784439,-0.64,0.15));
#22886=CARTESIAN_POINT('',(-0.0866025403784439,-0.4,0.15));
#22887=CARTESIAN_POINT('',(-0.173205080756888,-0.64,-2.12115047744981E-17));
#22888=CARTESIAN_POINT('Origin',(0.0866025403784439,-0.4,0.15));
#22889=CARTESIAN_POINT('',(0.0866025403784439,-0.4,0.15));
#22890=CARTESIAN_POINT('',(-0.0866025403784439,-0.4,0.15));
#22891=CARTESIAN_POINT('',(0.0866025403784439,-0.64,0.15));
#22892=CARTESIAN_POINT('',(0.0866025403784439,-0.4,0.15));
#22893=CARTESIAN_POINT('',(-0.0866025403784439,-0.64,0.15));
#22894=CARTESIAN_POINT('Origin',(0.173205080756888,-0.4,0.));
#22895=CARTESIAN_POINT('',(0.0866025403784439,-0.4,0.15));
#22896=CARTESIAN_POINT('',(0.0866025403784439,-0.64,0.15));
#22897=CARTESIAN_POINT('Origin',(0.,-0.4,-2.77555756156289E-17));
#22898=CARTESIAN_POINT('Origin',(0.,-0.64,-2.77555756156289E-17));
#23590=UNCERTAINTY_MEASURE_WITH_UNIT(LENGTH_MEASURE(0.001),#23729,
'DISTANCE_ACCURACY_VALUE',
'Maximum model space distance between geometric entities at asserted c
onnectivities');
#23611=UNCERTAINTY_MEASURE_WITH_UNIT(LENGTH_MEASURE(0.001),#23729,
'DISTANCE_ACCURACY_VALUE',
'Maximum model space distance between geometric entities at asserted c
onnectivities');
#23707=(
GEOMETRIC_REPRESENTATION_CONTEXT(3)
GLOBAL_UNCERTAINTY_ASSIGNED_CONTEXT((#23590))
GLOBAL_UNIT_ASSIGNED_CONTEXT((#23729,#23731,#23732))
REPRESENTATION_CONTEXT('','3D')
);
#23728=(
GEOMETRIC_REPRESENTATION_CONTEXT(3)
GLOBAL_UNCERTAINTY_ASSIGNED_CONTEXT((#23611))
GLOBAL_UNIT_ASSIGNED_CONTEXT((#23729,#23731,#23732))
REPRESENTATION_CONTEXT('','3D')
);
#23729=(
LENGTH_UNIT()
NAMED_UNIT(*)
SI_UNIT(.CENTI.,.METRE.)
);
#23731=(
NAMED_UNIT(*)
PLANE_ANGLE_UNIT()
SI_UNIT($,.RADIAN.)
);
#23732=(
NAMED_UNIT(*)
SI_UNIT($,.STERADIAN.)
SOLID_ANGLE_UNIT()
);
#23828=SHAPE_DEFINITION_REPRESENTATION(#23995,#24207);
#23995=PRODUCT_DEFINITION_SHAPE('',$,#24324);
#24207=SHAPE_REPRESENTATION('',(#15129),#23707);
#24228=PRODUCT_DEFINITION_CONTEXT('part definition',#24578,'design');
#24324=PRODUCT_DEFINITION('Cap Screw - M4x16','Cap Screw - M4x16',#24440,
#24228);
#24440=PRODUCT_DEFINITION_FORMATION('',$,#24675);
#24578=APPLICATION_CONTEXT(
'Core Data for Automotive Mechanical Design Process');
#24579=PRODUCT_CONTEXT('part definition',#24578,'mechanical');
#24675=PRODUCT('Cap Screw - M4x16','Cap Screw - M4x16',
'Cap Screw - M4x16',(#24579));
#24766=COLOUR_RGB('Black',0.12,0.14,0.17);
#24767=FILL_AREA_STYLE_COLOUR('',#24766);
#24768=FILL_AREA_STYLE('',(#24767));
#24769=SURFACE_STYLE_FILL_AREA(#24768);
#24770=SURFACE_SIDE_STYLE('',(#24769));
#24771=SURFACE_STYLE_USAGE(.BOTH.,#24770);
#24772=PRESENTATION_STYLE_ASSIGNMENT((#24771));
ENDSEC;
END-ISO-10303-21;
